ISO-10303-21;
HEADER;
/* Generated by software containing ST-Developer
 * from STEP Tools, Inc. (www.steptools.com) 
 */

FILE_DESCRIPTION(
/* description */ ('PAT-001'),
/* implementation_level */ '2;1');

FILE_NAME(
/* name */ 'Sliding axle block (1).step',
/* time_stamp */ '2026-10-29T17:07:15-07:00',
/* author */ (''),
/* organization */ (''),
/* preprocessor_version */ 'ST-DEVELOPER v20.2',
/* originating_system */ 'Autodesk Translation Framework v15.17.0.0',
/* authorisation */ '');

FILE_SCHEMA (('AUTOMOTIVE_DESIGN { 1 0 10303 214 3 1 1 }'));
ENDSEC;

DATA;
#10=MECHANICAL_DESIGN_GEOMETRIC_PRESENTATION_REPRESENTATION('',(#393),#9622);
#335=SHAPE_REPRESENTATION_RELATIONSHIP('SRR','None',#9759,#360);
#360=ADVANCED_BREP_SHAPE_REPRESENTATION('',(#426),#9608);
#393=STYLED_ITEM('',(#9962),#426);
#426=MANIFOLD_SOLID_BREP('Body1',#5218);
#471=FACE_BOUND('',#1161,.T.);
#472=FACE_BOUND('',#1166,.T.);
#473=FACE_BOUND('',#1182,.T.);
#474=FACE_BOUND('',#1183,.T.);
#475=FACE_BOUND('',#1184,.T.);
#476=FACE_BOUND('',#1185,.T.);
#477=FACE_BOUND('',#1186,.T.);
#478=FACE_BOUND('',#1188,.T.);
#479=FACE_BOUND('',#1189,.T.);
#584=PLANE('',#5764);
#585=PLANE('',#5765);
#586=PLANE('',#5767);
#587=PLANE('',#5768);
#588=PLANE('',#5770);
#589=PLANE('',#5771);
#590=PLANE('',#5781);
#591=PLANE('',#5782);
#592=PLANE('',#5783);
#593=PLANE('',#5788);
#594=PLANE('',#5789);
#595=PLANE('',#5790);
#596=PLANE('',#5791);
#597=PLANE('',#5792);
#598=PLANE('',#5793);
#599=PLANE('',#5794);
#600=PLANE('',#5795);
#827=FACE_OUTER_BOUND('',#1157,.T.);
#828=FACE_OUTER_BOUND('',#1158,.T.);
#829=FACE_OUTER_BOUND('',#1159,.T.);
#830=FACE_OUTER_BOUND('',#1160,.T.);
#831=FACE_OUTER_BOUND('',#1162,.T.);
#832=FACE_OUTER_BOUND('',#1163,.T.);
#833=FACE_OUTER_BOUND('',#1164,.T.);
#834=FACE_OUTER_BOUND('',#1165,.T.);
#835=FACE_OUTER_BOUND('',#1167,.T.);
#836=FACE_OUTER_BOUND('',#1168,.T.);
#837=FACE_OUTER_BOUND('',#1169,.T.);
#838=FACE_OUTER_BOUND('',#1170,.T.);
#839=FACE_OUTER_BOUND('',#1171,.T.);
#840=FACE_OUTER_BOUND('',#1172,.T.);
#841=FACE_OUTER_BOUND('',#1173,.T.);
#842=FACE_OUTER_BOUND('',#1174,.T.);
#843=FACE_OUTER_BOUND('',#1175,.T.);
#844=FACE_OUTER_BOUND('',#1176,.T.);
#845=FACE_OUTER_BOUND('',#1177,.T.);
#846=FACE_OUTER_BOUND('',#1178,.T.);
#847=FACE_OUTER_BOUND('',#1179,.T.);
#848=FACE_OUTER_BOUND('',#1180,.T.);
#849=FACE_OUTER_BOUND('',#1181,.T.);
#850=FACE_OUTER_BOUND('',#1187,.T.);
#1157=EDGE_LOOP('',(#3969,#3970,#3971,#3972));
#1158=EDGE_LOOP('',(#3973,#3974,#3975,#3976));
#1159=EDGE_LOOP('',(#3977,#3978,#3979,#3980));
#1160=EDGE_LOOP('',(#3981,#3982,#3983,#3984));
#1161=EDGE_LOOP('',(#3985));
#1162=EDGE_LOOP('',(#3986,#3987,#3988,#3989));
#1163=EDGE_LOOP('',(#3990,#3991,#3992,#3993));
#1164=EDGE_LOOP('',(#3994,#3995,#3996,#3997));
#1165=EDGE_LOOP('',(#3998,#3999,#4000,#4001));
#1166=EDGE_LOOP('',(#4002));
#1167=EDGE_LOOP('',(#4003,#4004,#4005,#4006));
#1168=EDGE_LOOP('',(#4007,#4008,#4009,#4010));
#1169=EDGE_LOOP('',(#4011,#4012,#4013,#4014));
#1170=EDGE_LOOP('',(#4015,#4016,#4017,#4018));
#1171=EDGE_LOOP('',(#4019,#4020,#4021,#4022));
#1172=EDGE_LOOP('',(#4023,#4024,#4025,#4026));
#1173=EDGE_LOOP('',(#4027,#4028,#4029,#4030));
#1174=EDGE_LOOP('',(#4031,#4032,#4033,#4034));
#1175=EDGE_LOOP('',(#4035,#4036,#4037,#4038));
#1176=EDGE_LOOP('',(#4039,#4040,#4041,#4042));
#1177=EDGE_LOOP('',(#4043,#4044,#4045,#4046));
#1178=EDGE_LOOP('',(#4047,#4048,#4049,#4050));
#1179=EDGE_LOOP('',(#4051,#4052,#4053,#4054));
#1180=EDGE_LOOP('',(#4055,#4056,#4057,#4058));
#1181=EDGE_LOOP('',(#4059,#4060,#4061,#4062));
#1182=EDGE_LOOP('',(#4063,#4064,#4065,#4066));
#1183=EDGE_LOOP('',(#4067));
#1184=EDGE_LOOP('',(#4068,#4069,#4070,#4071));
#1185=EDGE_LOOP('',(#4072));
#1186=EDGE_LOOP('',(#4073,#4074,#4075,#4076));
#1187=EDGE_LOOP('',(#4077,#4078,#4079,#4080));
#1188=EDGE_LOOP('',(#4081));
#1189=EDGE_LOOP('',(#4082));
#1490=LINE('',#8568,#1895);
#1491=LINE('',#8572,#1896);
#1492=LINE('',#8577,#1897);
#1493=LINE('',#8581,#1898);
#1494=LINE('',#8585,#1899);
#1495=LINE('',#8587,#1900);
#1496=LINE('',#8588,#1901);
#1497=LINE('',#8591,#1902);
#1498=LINE('',#8593,#1903);
#1499=LINE('',#8594,#1904);
#1500=LINE('',#8599,#1905);
#1501=LINE('',#8600,#1906);
#1502=LINE('',#8603,#1907);
#1503=LINE('',#8607,#1908);
#1504=LINE('',#8608,#1909);
#1505=LINE('',#8611,#1910);
#1506=LINE('',#8612,#1911);
#1507=LINE('',#8619,#1912);
#1508=LINE('',#8624,#1913);
#1509=LINE('',#8628,#1914);
#1510=LINE('',#8634,#1915);
#1511=LINE('',#8636,#1916);
#1512=LINE('',#8637,#1917);
#1513=LINE('',#8640,#1918);
#1514=LINE('',#8641,#1919);
#1515=LINE('',#8644,#1920);
#1516=LINE('',#8645,#1921);
#1517=LINE('',#8650,#1922);
#1518=LINE('',#8653,#1923);
#1519=LINE('',#8655,#1924);
#1520=LINE('',#8657,#1925);
#1521=LINE('',#8661,#1926);
#1522=LINE('',#8663,#1927);
#1523=LINE('',#8665,#1928);
#1524=LINE('',#8666,#1929);
#1525=LINE('',#8669,#1930);
#1526=LINE('',#8671,#1931);
#1527=LINE('',#8672,#1932);
#1528=LINE('',#8675,#1933);
#1529=LINE('',#8677,#1934);
#1530=LINE('',#8678,#1935);
#1531=LINE('',#8680,#1936);
#1532=LINE('',#8681,#1937);
#1895=VECTOR('',#6699,1.);
#1896=VECTOR('',#6702,1.);
#1897=VECTOR('',#6707,1.);
#1898=VECTOR('',#6710,1.);
#1899=VECTOR('',#6715,1.);
#1900=VECTOR('',#6716,1.);
#1901=VECTOR('',#6717,1.);
#1902=VECTOR('',#6720,1.);
#1903=VECTOR('',#6721,1.);
#1904=VECTOR('',#6722,1.);
#1905=VECTOR('',#6727,1.);
#1906=VECTOR('',#6728,1.);
#1907=VECTOR('',#6731,1.);
#1908=VECTOR('',#6736,1.);
#1909=VECTOR('',#6737,1.);
#1910=VECTOR('',#6740,1.);
#1911=VECTOR('',#6741,1.);
#1912=VECTOR('',#6748,0.275);
#1913=VECTOR('',#6753,1.);
#1914=VECTOR('',#6756,1.);
#1915=VECTOR('',#6765,1.);
#1916=VECTOR('',#6766,1.);
#1917=VECTOR('',#6767,1.);
#1918=VECTOR('',#6770,1.);
#1919=VECTOR('',#6771,1.);
#1920=VECTOR('',#6774,1.);
#1921=VECTOR('',#6775,1.);
#1922=VECTOR('',#6780,0.275);
#1923=VECTOR('',#6785,0.505);
#1924=VECTOR('',#6788,1.);
#1925=VECTOR('',#6791,1.);
#1926=VECTOR('',#6794,1.);
#1927=VECTOR('',#6795,1.);
#1928=VECTOR('',#6796,1.);
#1929=VECTOR('',#6797,1.);
#1930=VECTOR('',#6800,1.);
#1931=VECTOR('',#6801,1.);
#1932=VECTOR('',#6802,1.);
#1933=VECTOR('',#6805,1.);
#1934=VECTOR('',#6806,1.);
#1935=VECTOR('',#6807,1.);
#1936=VECTOR('',#6810,1.);
#1937=VECTOR('',#6811,1.);
#2324=CIRCLE('',#5759,0.525);
#2325=CIRCLE('',#5760,0.525);
#2326=CIRCLE('',#5762,0.525);
#2327=CIRCLE('',#5763,0.525);
#2328=CIRCLE('',#5766,0.505);
#2329=CIRCLE('',#5769,0.525);
#2330=CIRCLE('',#5772,0.505);
#2331=CIRCLE('',#5774,0.275);
#2332=CIRCLE('',#5775,0.275);
#2333=CIRCLE('',#5777,0.525);
#2334=CIRCLE('',#5778,0.525);
#2335=CIRCLE('',#5780,0.525);
#2336=CIRCLE('',#5785,0.275);
#2337=CIRCLE('',#5786,0.275);
#2580=VERTEX_POINT('',#8566);
#2581=VERTEX_POINT('',#8567);
#2582=VERTEX_POINT('',#8569);
#2583=VERTEX_POINT('',#8571);
#2584=VERTEX_POINT('',#8575);
#2585=VERTEX_POINT('',#8576);
#2586=VERTEX_POINT('',#8578);
#2587=VERTEX_POINT('',#8580);
#2588=VERTEX_POINT('',#8584);
#2589=VERTEX_POINT('',#8586);
#2590=VERTEX_POINT('',#8590);
#2591=VERTEX_POINT('',#8592);
#2592=VERTEX_POINT('',#8595);
#2593=VERTEX_POINT('',#8598);
#2594=VERTEX_POINT('',#8602);
#2595=VERTEX_POINT('',#8606);
#2596=VERTEX_POINT('',#8610);
#2597=VERTEX_POINT('',#8613);
#2598=VERTEX_POINT('',#8616);
#2599=VERTEX_POINT('',#8618);
#2600=VERTEX_POINT('',#8622);
#2601=VERTEX_POINT('',#8623);
#2602=VERTEX_POINT('',#8625);
#2603=VERTEX_POINT('',#8627);
#2604=VERTEX_POINT('',#8633);
#2605=VERTEX_POINT('',#8635);
#2606=VERTEX_POINT('',#8639);
#2607=VERTEX_POINT('',#8643);
#2608=VERTEX_POINT('',#8647);
#2609=VERTEX_POINT('',#8649);
#2610=VERTEX_POINT('',#8659);
#2611=VERTEX_POINT('',#8660);
#2612=VERTEX_POINT('',#8662);
#2613=VERTEX_POINT('',#8664);
#2614=VERTEX_POINT('',#8668);
#2615=VERTEX_POINT('',#8670);
#2616=VERTEX_POINT('',#8674);
#2617=VERTEX_POINT('',#8676);
#3088=EDGE_CURVE('',#2580,#2581,#1490,.T.);
#3089=EDGE_CURVE('',#2582,#2580,#2324,.T.);
#3090=EDGE_CURVE('',#2583,#2582,#1491,.T.);
#3091=EDGE_CURVE('',#2581,#2583,#2325,.T.);
#3092=EDGE_CURVE('',#2584,#2585,#1492,.T.);
#3093=EDGE_CURVE('',#2586,#2584,#2326,.T.);
#3094=EDGE_CURVE('',#2587,#2586,#1493,.T.);
#3095=EDGE_CURVE('',#2585,#2587,#2327,.T.);
#3096=EDGE_CURVE('',#2588,#2581,#1494,.T.);
#3097=EDGE_CURVE('',#2588,#2589,#1495,.T.);
#3098=EDGE_CURVE('',#2589,#2580,#1496,.T.);
#3099=EDGE_CURVE('',#2585,#2590,#1497,.T.);
#3100=EDGE_CURVE('',#2590,#2591,#1498,.T.);
#3101=EDGE_CURVE('',#2584,#2591,#1499,.T.);
#3102=EDGE_CURVE('',#2592,#2592,#2328,.T.);
#3103=EDGE_CURVE('',#2589,#2593,#1500,.T.);
#3104=EDGE_CURVE('',#2582,#2593,#1501,.T.);
#3105=EDGE_CURVE('',#2594,#2587,#1502,.T.);
#3106=EDGE_CURVE('',#2594,#2590,#2329,.T.);
#3107=EDGE_CURVE('',#2593,#2595,#1503,.T.);
#3108=EDGE_CURVE('',#2583,#2595,#1504,.T.);
#3109=EDGE_CURVE('',#2596,#2586,#1505,.T.);
#3110=EDGE_CURVE('',#2596,#2594,#1506,.T.);
#3111=EDGE_CURVE('',#2597,#2597,#2330,.T.);
#3112=EDGE_CURVE('',#2598,#2598,#2331,.T.);
#3113=EDGE_CURVE('',#2598,#2599,#1507,.T.);
#3114=EDGE_CURVE('',#2599,#2599,#2332,.T.);
#3115=EDGE_CURVE('',#2600,#2601,#1508,.T.);
#3116=EDGE_CURVE('',#2602,#2600,#2333,.T.);
#3117=EDGE_CURVE('',#2603,#2602,#1509,.T.);
#3118=EDGE_CURVE('',#2601,#2603,#2334,.T.);
#3119=EDGE_CURVE('',#2591,#2596,#2335,.T.);
#3120=EDGE_CURVE('',#2604,#2601,#1510,.T.);
#3121=EDGE_CURVE('',#2604,#2605,#1511,.T.);
#3122=EDGE_CURVE('',#2605,#2600,#1512,.T.);
#3123=EDGE_CURVE('',#2606,#2605,#1513,.T.);
#3124=EDGE_CURVE('',#2602,#2606,#1514,.T.);
#3125=EDGE_CURVE('',#2606,#2607,#1515,.T.);
#3126=EDGE_CURVE('',#2603,#2607,#1516,.T.);
#3127=EDGE_CURVE('',#2608,#2608,#2336,.T.);
#3128=EDGE_CURVE('',#2608,#2609,#1517,.T.);
#3129=EDGE_CURVE('',#2609,#2609,#2337,.T.);
#3130=EDGE_CURVE('',#2592,#2597,#1518,.T.);
#3131=EDGE_CURVE('',#2595,#2588,#1519,.T.);
#3132=EDGE_CURVE('',#2607,#2604,#1520,.T.);
#3133=EDGE_CURVE('',#2610,#2611,#1521,.T.);
#3134=EDGE_CURVE('',#2611,#2612,#1522,.T.);
#3135=EDGE_CURVE('',#2613,#2612,#1523,.T.);
#3136=EDGE_CURVE('',#2610,#2613,#1524,.T.);
#3137=EDGE_CURVE('',#2614,#2610,#1525,.T.);
#3138=EDGE_CURVE('',#2615,#2613,#1526,.T.);
#3139=EDGE_CURVE('',#2614,#2615,#1527,.T.);
#3140=EDGE_CURVE('',#2616,#2614,#1528,.T.);
#3141=EDGE_CURVE('',#2617,#2615,#1529,.T.);
#3142=EDGE_CURVE('',#2616,#2617,#1530,.T.);
#3143=EDGE_CURVE('',#2611,#2616,#1531,.T.);
#3144=EDGE_CURVE('',#2612,#2617,#1532,.T.);
#3969=ORIENTED_EDGE('',*,*,#3088,.F.);
#3970=ORIENTED_EDGE('',*,*,#3089,.F.);
#3971=ORIENTED_EDGE('',*,*,#3090,.F.);
#3972=ORIENTED_EDGE('',*,*,#3091,.F.);
#3973=ORIENTED_EDGE('',*,*,#3092,.F.);
#3974=ORIENTED_EDGE('',*,*,#3093,.F.);
#3975=ORIENTED_EDGE('',*,*,#3094,.F.);
#3976=ORIENTED_EDGE('',*,*,#3095,.F.);
#3977=ORIENTED_EDGE('',*,*,#3088,.T.);
#3978=ORIENTED_EDGE('',*,*,#3096,.F.);
#3979=ORIENTED_EDGE('',*,*,#3097,.T.);
#3980=ORIENTED_EDGE('',*,*,#3098,.T.);
#3981=ORIENTED_EDGE('',*,*,#3092,.T.);
#3982=ORIENTED_EDGE('',*,*,#3099,.T.);
#3983=ORIENTED_EDGE('',*,*,#3100,.T.);
#3984=ORIENTED_EDGE('',*,*,#3101,.F.);
#3985=ORIENTED_EDGE('',*,*,#3102,.T.);
#3986=ORIENTED_EDGE('',*,*,#3089,.T.);
#3987=ORIENTED_EDGE('',*,*,#3098,.F.);
#3988=ORIENTED_EDGE('',*,*,#3103,.T.);
#3989=ORIENTED_EDGE('',*,*,#3104,.F.);
#3990=ORIENTED_EDGE('',*,*,#3095,.T.);
#3991=ORIENTED_EDGE('',*,*,#3105,.F.);
#3992=ORIENTED_EDGE('',*,*,#3106,.T.);
#3993=ORIENTED_EDGE('',*,*,#3099,.F.);
#3994=ORIENTED_EDGE('',*,*,#3090,.T.);
#3995=ORIENTED_EDGE('',*,*,#3104,.T.);
#3996=ORIENTED_EDGE('',*,*,#3107,.T.);
#3997=ORIENTED_EDGE('',*,*,#3108,.F.);
#3998=ORIENTED_EDGE('',*,*,#3094,.T.);
#3999=ORIENTED_EDGE('',*,*,#3109,.F.);
#4000=ORIENTED_EDGE('',*,*,#3110,.T.);
#4001=ORIENTED_EDGE('',*,*,#3105,.T.);
#4002=ORIENTED_EDGE('',*,*,#3111,.T.);
#4003=ORIENTED_EDGE('',*,*,#3112,.F.);
#4004=ORIENTED_EDGE('',*,*,#3113,.T.);
#4005=ORIENTED_EDGE('',*,*,#3114,.T.);
#4006=ORIENTED_EDGE('',*,*,#3113,.F.);
#4007=ORIENTED_EDGE('',*,*,#3115,.F.);
#4008=ORIENTED_EDGE('',*,*,#3116,.F.);
#4009=ORIENTED_EDGE('',*,*,#3117,.F.);
#4010=ORIENTED_EDGE('',*,*,#3118,.F.);
#4011=ORIENTED_EDGE('',*,*,#3110,.F.);
#4012=ORIENTED_EDGE('',*,*,#3119,.F.);
#4013=ORIENTED_EDGE('',*,*,#3100,.F.);
#4014=ORIENTED_EDGE('',*,*,#3106,.F.);
#4015=ORIENTED_EDGE('',*,*,#3115,.T.);
#4016=ORIENTED_EDGE('',*,*,#3120,.F.);
#4017=ORIENTED_EDGE('',*,*,#3121,.T.);
#4018=ORIENTED_EDGE('',*,*,#3122,.T.);
#4019=ORIENTED_EDGE('',*,*,#3116,.T.);
#4020=ORIENTED_EDGE('',*,*,#3122,.F.);
#4021=ORIENTED_EDGE('',*,*,#3123,.F.);
#4022=ORIENTED_EDGE('',*,*,#3124,.F.);
#4023=ORIENTED_EDGE('',*,*,#3117,.T.);
#4024=ORIENTED_EDGE('',*,*,#3124,.T.);
#4025=ORIENTED_EDGE('',*,*,#3125,.T.);
#4026=ORIENTED_EDGE('',*,*,#3126,.F.);
#4027=ORIENTED_EDGE('',*,*,#3127,.F.);
#4028=ORIENTED_EDGE('',*,*,#3128,.T.);
#4029=ORIENTED_EDGE('',*,*,#3129,.T.);
#4030=ORIENTED_EDGE('',*,*,#3128,.F.);
#4031=ORIENTED_EDGE('',*,*,#3102,.F.);
#4032=ORIENTED_EDGE('',*,*,#3130,.T.);
#4033=ORIENTED_EDGE('',*,*,#3111,.F.);
#4034=ORIENTED_EDGE('',*,*,#3130,.F.);
#4035=ORIENTED_EDGE('',*,*,#3131,.F.);
#4036=ORIENTED_EDGE('',*,*,#3107,.F.);
#4037=ORIENTED_EDGE('',*,*,#3103,.F.);
#4038=ORIENTED_EDGE('',*,*,#3097,.F.);
#4039=ORIENTED_EDGE('',*,*,#3132,.F.);
#4040=ORIENTED_EDGE('',*,*,#3125,.F.);
#4041=ORIENTED_EDGE('',*,*,#3123,.T.);
#4042=ORIENTED_EDGE('',*,*,#3121,.F.);
#4043=ORIENTED_EDGE('',*,*,#3133,.T.);
#4044=ORIENTED_EDGE('',*,*,#3134,.T.);
#4045=ORIENTED_EDGE('',*,*,#3135,.F.);
#4046=ORIENTED_EDGE('',*,*,#3136,.F.);
#4047=ORIENTED_EDGE('',*,*,#3137,.T.);
#4048=ORIENTED_EDGE('',*,*,#3136,.T.);
#4049=ORIENTED_EDGE('',*,*,#3138,.F.);
#4050=ORIENTED_EDGE('',*,*,#3139,.F.);
#4051=ORIENTED_EDGE('',*,*,#3140,.T.);
#4052=ORIENTED_EDGE('',*,*,#3139,.T.);
#4053=ORIENTED_EDGE('',*,*,#3141,.F.);
#4054=ORIENTED_EDGE('',*,*,#3142,.F.);
#4055=ORIENTED_EDGE('',*,*,#3143,.T.);
#4056=ORIENTED_EDGE('',*,*,#3142,.T.);
#4057=ORIENTED_EDGE('',*,*,#3144,.F.);
#4058=ORIENTED_EDGE('',*,*,#3134,.F.);
#4059=ORIENTED_EDGE('',*,*,#3144,.T.);
#4060=ORIENTED_EDGE('',*,*,#3141,.T.);
#4061=ORIENTED_EDGE('',*,*,#3138,.T.);
#4062=ORIENTED_EDGE('',*,*,#3135,.T.);
#4063=ORIENTED_EDGE('',*,*,#3101,.T.);
#4064=ORIENTED_EDGE('',*,*,#3119,.T.);
#4065=ORIENTED_EDGE('',*,*,#3109,.T.);
#4066=ORIENTED_EDGE('',*,*,#3093,.T.);
#4067=ORIENTED_EDGE('',*,*,#3114,.F.);
#4068=ORIENTED_EDGE('',*,*,#3091,.T.);
#4069=ORIENTED_EDGE('',*,*,#3108,.T.);
#4070=ORIENTED_EDGE('',*,*,#3131,.T.);
#4071=ORIENTED_EDGE('',*,*,#3096,.T.);
#4072=ORIENTED_EDGE('',*,*,#3129,.F.);
#4073=ORIENTED_EDGE('',*,*,#3118,.T.);
#4074=ORIENTED_EDGE('',*,*,#3126,.T.);
#4075=ORIENTED_EDGE('',*,*,#3132,.T.);
#4076=ORIENTED_EDGE('',*,*,#3120,.T.);
#4077=ORIENTED_EDGE('',*,*,#3143,.F.);
#4078=ORIENTED_EDGE('',*,*,#3133,.F.);
#4079=ORIENTED_EDGE('',*,*,#3137,.F.);
#4080=ORIENTED_EDGE('',*,*,#3140,.F.);
#4081=ORIENTED_EDGE('',*,*,#3112,.T.);
#4082=ORIENTED_EDGE('',*,*,#3127,.T.);
#4861=CYLINDRICAL_SURFACE('',#5758,0.525);
#4862=CYLINDRICAL_SURFACE('',#5761,0.525);
#4863=CYLINDRICAL_SURFACE('',#5773,0.275);
#4864=CYLINDRICAL_SURFACE('',#5776,0.525);
#4865=CYLINDRICAL_SURFACE('',#5779,0.525);
#4866=CYLINDRICAL_SURFACE('',#5784,0.275);
#4867=CYLINDRICAL_SURFACE('',#5787,0.505);
#5014=ADVANCED_FACE('',(#827),#4861,.F.);
#5015=ADVANCED_FACE('',(#828),#4862,.F.);
#5016=ADVANCED_FACE('',(#829),#584,.F.);
#5017=ADVANCED_FACE('',(#830,#471),#585,.F.);
#5018=ADVANCED_FACE('',(#831),#586,.T.);
#5019=ADVANCED_FACE('',(#832),#587,.T.);
#5020=ADVANCED_FACE('',(#833),#588,.T.);
#5021=ADVANCED_FACE('',(#834,#472),#589,.T.);
#5022=ADVANCED_FACE('',(#835),#4863,.F.);
#5023=ADVANCED_FACE('',(#836),#4864,.F.);
#5024=ADVANCED_FACE('',(#837),#4865,.F.);
#5025=ADVANCED_FACE('',(#838),#590,.T.);
#5026=ADVANCED_FACE('',(#839),#591,.T.);
#5027=ADVANCED_FACE('',(#840),#592,.F.);
#5028=ADVANCED_FACE('',(#841),#4866,.F.);
#5029=ADVANCED_FACE('',(#842),#4867,.F.);
#5030=ADVANCED_FACE('',(#843),#593,.T.);
#5031=ADVANCED_FACE('',(#844),#594,.T.);
#5032=ADVANCED_FACE('',(#845),#595,.T.);
#5033=ADVANCED_FACE('',(#846),#596,.T.);
#5034=ADVANCED_FACE('',(#847),#597,.T.);
#5035=ADVANCED_FACE('',(#848),#598,.T.);
#5036=ADVANCED_FACE('',(#849,#473,#474,#475,#476,#477),#599,.T.);
#5037=ADVANCED_FACE('',(#850,#478,#479),#600,.F.);
#5218=CLOSED_SHELL('',(#5014,#5015,#5016,#5017,#5018,#5019,#5020,#5021,
#5022,#5023,#5024,#5025,#5026,#5027,#5028,#5029,#5030,#5031,#5032,#5033,
#5034,#5035,#5036,#5037));
#5757=AXIS2_PLACEMENT_3D('',#8564,#6695,#6696);
#5758=AXIS2_PLACEMENT_3D('',#8565,#6697,#6698);
#5759=AXIS2_PLACEMENT_3D('',#8570,#6700,#6701);
#5760=AXIS2_PLACEMENT_3D('',#8573,#6703,#6704);
#5761=AXIS2_PLACEMENT_3D('',#8574,#6705,#6706);
#5762=AXIS2_PLACEMENT_3D('',#8579,#6708,#6709);
#5763=AXIS2_PLACEMENT_3D('',#8582,#6711,#6712);
#5764=AXIS2_PLACEMENT_3D('',#8583,#6713,#6714);
#5765=AXIS2_PLACEMENT_3D('',#8589,#6718,#6719);
#5766=AXIS2_PLACEMENT_3D('',#8596,#6723,#6724);
#5767=AXIS2_PLACEMENT_3D('',#8597,#6725,#6726);
#5768=AXIS2_PLACEMENT_3D('',#8601,#6729,#6730);
#5769=AXIS2_PLACEMENT_3D('',#8604,#6732,#6733);
#5770=AXIS2_PLACEMENT_3D('',#8605,#6734,#6735);
#5771=AXIS2_PLACEMENT_3D('',#8609,#6738,#6739);
#5772=AXIS2_PLACEMENT_3D('',#8614,#6742,#6743);
#5773=AXIS2_PLACEMENT_3D('',#8615,#6744,#6745);
#5774=AXIS2_PLACEMENT_3D('',#8617,#6746,#6747);
#5775=AXIS2_PLACEMENT_3D('',#8620,#6749,#6750);
#5776=AXIS2_PLACEMENT_3D('',#8621,#6751,#6752);
#5777=AXIS2_PLACEMENT_3D('',#8626,#6754,#6755);
#5778=AXIS2_PLACEMENT_3D('',#8629,#6757,#6758);
#5779=AXIS2_PLACEMENT_3D('',#8630,#6759,#6760);
#5780=AXIS2_PLACEMENT_3D('',#8631,#6761,#6762);
#5781=AXIS2_PLACEMENT_3D('',#8632,#6763,#6764);
#5782=AXIS2_PLACEMENT_3D('',#8638,#6768,#6769);
#5783=AXIS2_PLACEMENT_3D('',#8642,#6772,#6773);
#5784=AXIS2_PLACEMENT_3D('',#8646,#6776,#6777);
#5785=AXIS2_PLACEMENT_3D('',#8648,#6778,#6779);
#5786=AXIS2_PLACEMENT_3D('',#8651,#6781,#6782);
#5787=AXIS2_PLACEMENT_3D('',#8652,#6783,#6784);
#5788=AXIS2_PLACEMENT_3D('',#8654,#6786,#6787);
#5789=AXIS2_PLACEMENT_3D('',#8656,#6789,#6790);
#5790=AXIS2_PLACEMENT_3D('',#8658,#6792,#6793);
#5791=AXIS2_PLACEMENT_3D('',#8667,#6798,#6799);
#5792=AXIS2_PLACEMENT_3D('',#8673,#6803,#6804);
#5793=AXIS2_PLACEMENT_3D('',#8679,#6808,#6809);
#5794=AXIS2_PLACEMENT_3D('',#8682,#6812,#6813);
#5795=AXIS2_PLACEMENT_3D('',#8683,#6814,#6815);
#6695=DIRECTION('axis',(0.,0.,1.));
#6696=DIRECTION('refdir',(1.,0.,0.));
#6697=DIRECTION('center_axis',(0.,0.,1.));
#6698=DIRECTION('ref_axis',(1.,0.,0.));
#6699=DIRECTION('',(0.,0.,-1.));
#6700=DIRECTION('center_axis',(0.,0.,-1.));
#6701=DIRECTION('ref_axis',(1.,0.,0.));
#6702=DIRECTION('',(0.,0.,1.));
#6703=DIRECTION('center_axis',(0.,0.,1.));
#6704=DIRECTION('ref_axis',(1.,0.,0.));
#6705=DIRECTION('center_axis',(0.,0.,1.));
#6706=DIRECTION('ref_axis',(-1.,-1.22464679914735E-16,0.));
#6707=DIRECTION('',(0.,0.,1.));
#6708=DIRECTION('center_axis',(0.,0.,1.));
#6709=DIRECTION('ref_axis',(1.,0.,0.));
#6710=DIRECTION('',(0.,0.,-1.));
#6711=DIRECTION('center_axis',(0.,0.,-1.));
#6712=DIRECTION('ref_axis',(1.,0.,0.));
#6713=DIRECTION('center_axis',(0.,1.,0.));
#6714=DIRECTION('ref_axis',(1.,0.,0.));
#6715=DIRECTION('',(-1.,0.,0.));
#6716=DIRECTION('',(0.,0.,1.));
#6717=DIRECTION('',(-1.,0.,0.));
#6718=DIRECTION('center_axis',(0.,1.,0.));
#6719=DIRECTION('ref_axis',(1.,0.,0.));
#6720=DIRECTION('',(-1.,0.,0.));
#6721=DIRECTION('',(0.,0.,-1.));
#6722=DIRECTION('',(-1.,0.,0.));
#6723=DIRECTION('center_axis',(0.,1.,0.));
#6724=DIRECTION('ref_axis',(1.,0.,0.));
#6725=DIRECTION('center_axis',(0.,0.,1.));
#6726=DIRECTION('ref_axis',(1.,0.,0.));
#6727=DIRECTION('',(0.,1.,0.));
#6728=DIRECTION('',(1.,0.,0.));
#6729=DIRECTION('center_axis',(0.,0.,1.));
#6730=DIRECTION('ref_axis',(1.,0.,0.));
#6731=DIRECTION('',(1.,0.,0.));
#6732=DIRECTION('center_axis',(0.,0.,-1.));
#6733=DIRECTION('ref_axis',(1.,0.,0.));
#6734=DIRECTION('center_axis',(0.,1.,0.));
#6735=DIRECTION('ref_axis',(0.,0.,1.));
#6736=DIRECTION('',(0.,0.,-1.));
#6737=DIRECTION('',(1.,0.,0.));
#6738=DIRECTION('center_axis',(0.,1.,0.));
#6739=DIRECTION('ref_axis',(0.,0.,1.));
#6740=DIRECTION('',(1.,0.,0.));
#6741=DIRECTION('',(0.,0.,1.));
#6742=DIRECTION('center_axis',(0.,-1.,0.));
#6743=DIRECTION('ref_axis',(1.,0.,0.));
#6744=DIRECTION('center_axis',(0.,0.,1.));
#6745=DIRECTION('ref_axis',(1.,0.,0.));
#6746=DIRECTION('center_axis',(0.,0.,1.));
#6747=DIRECTION('ref_axis',(1.,0.,0.));
#6748=DIRECTION('',(0.,0.,1.));
#6749=DIRECTION('center_axis',(0.,0.,1.));
#6750=DIRECTION('ref_axis',(1.,0.,0.));
#6751=DIRECTION('center_axis',(0.,0.,1.));
#6752=DIRECTION('ref_axis',(-1.,1.22464679914735E-16,0.));
#6753=DIRECTION('',(0.,0.,-1.));
#6754=DIRECTION('center_axis',(0.,0.,-1.));
#6755=DIRECTION('ref_axis',(1.,0.,0.));
#6756=DIRECTION('',(0.,0.,1.));
#6757=DIRECTION('center_axis',(0.,0.,1.));
#6758=DIRECTION('ref_axis',(1.,0.,0.));
#6759=DIRECTION('center_axis',(0.,0.,1.));
#6760=DIRECTION('ref_axis',(1.,0.,0.));
#6761=DIRECTION('center_axis',(0.,0.,1.));
#6762=DIRECTION('ref_axis',(1.,0.,0.));
#6763=DIRECTION('center_axis',(0.,1.,0.));
#6764=DIRECTION('ref_axis',(0.,0.,1.));
#6765=DIRECTION('',(1.,0.,0.));
#6766=DIRECTION('',(0.,0.,1.));
#6767=DIRECTION('',(1.,0.,0.));
#6768=DIRECTION('center_axis',(0.,0.,1.));
#6769=DIRECTION('ref_axis',(1.,0.,0.));
#6770=DIRECTION('',(0.,1.,0.));
#6771=DIRECTION('',(-1.,0.,0.));
#6772=DIRECTION('center_axis',(0.,1.,0.));
#6773=DIRECTION('ref_axis',(1.,0.,0.));
#6774=DIRECTION('',(0.,0.,-1.));
#6775=DIRECTION('',(-1.,0.,0.));
#6776=DIRECTION('center_axis',(0.,0.,1.));
#6777=DIRECTION('ref_axis',(1.,0.,0.));
#6778=DIRECTION('center_axis',(0.,0.,1.));
#6779=DIRECTION('ref_axis',(1.,0.,0.));
#6780=DIRECTION('',(0.,0.,1.));
#6781=DIRECTION('center_axis',(0.,0.,1.));
#6782=DIRECTION('ref_axis',(1.,0.,0.));
#6783=DIRECTION('center_axis',(0.,1.,0.));
#6784=DIRECTION('ref_axis',(1.,0.,0.));
#6785=DIRECTION('',(0.,1.,0.));
#6786=DIRECTION('center_axis',(1.,0.,0.));
#6787=DIRECTION('ref_axis',(0.,0.,-1.));
#6788=DIRECTION('',(0.,-1.,0.));
#6789=DIRECTION('center_axis',(-1.,0.,0.));
#6790=DIRECTION('ref_axis',(0.,0.,1.));
#6791=DIRECTION('',(0.,1.,0.));
#6792=DIRECTION('center_axis',(0.,1.,0.));
#6793=DIRECTION('ref_axis',(-1.,0.,0.));
#6794=DIRECTION('',(-1.,0.,0.));
#6795=DIRECTION('',(0.,0.,1.));
#6796=DIRECTION('',(-1.,0.,0.));
#6797=DIRECTION('',(0.,0.,1.));
#6798=DIRECTION('center_axis',(1.,0.,0.));
#6799=DIRECTION('ref_axis',(0.,1.,0.));
#6800=DIRECTION('',(0.,1.,0.));
#6801=DIRECTION('',(0.,1.,0.));
#6802=DIRECTION('',(0.,0.,1.));
#6803=DIRECTION('center_axis',(0.,-1.,0.));
#6804=DIRECTION('ref_axis',(1.,0.,0.));
#6805=DIRECTION('',(1.,0.,0.));
#6806=DIRECTION('',(1.,0.,0.));
#6807=DIRECTION('',(0.,0.,1.));
#6808=DIRECTION('center_axis',(-1.,0.,0.));
#6809=DIRECTION('ref_axis',(0.,-1.,0.));
#6810=DIRECTION('',(0.,-1.,0.));
#6811=DIRECTION('',(0.,-1.,0.));
#6812=DIRECTION('center_axis',(0.,0.,1.));
#6813=DIRECTION('ref_axis',(1.,0.,0.));
#6814=DIRECTION('center_axis',(0.,0.,1.));
#6815=DIRECTION('ref_axis',(1.,0.,0.));
#8564=CARTESIAN_POINT('',(0.,0.,0.));
#8565=CARTESIAN_POINT('Origin',(1.5,32.,2.8));
#8566=CARTESIAN_POINT('',(1.84003676271839,31.6,6.5));
#8567=CARTESIAN_POINT('',(1.84003676271839,31.6,2.8));
#8568=CARTESIAN_POINT('',(1.84003676271839,31.6,2.8));
#8569=CARTESIAN_POINT('',(1.84003676271839,32.4,6.5));
#8570=CARTESIAN_POINT('Origin',(1.5,32.,6.5));
#8571=CARTESIAN_POINT('',(1.84003676271839,32.4,2.8));
#8572=CARTESIAN_POINT('',(1.84003676271839,32.4,2.8));
#8573=CARTESIAN_POINT('Origin',(1.5,32.,2.8));
#8574=CARTESIAN_POINT('Origin',(1.5,32.,2.8));
#8575=CARTESIAN_POINT('',(1.15996323728161,31.6,2.8));
#8576=CARTESIAN_POINT('',(1.15996323728161,31.6,6.5));
#8577=CARTESIAN_POINT('',(1.15996323728161,31.6,2.8));
#8578=CARTESIAN_POINT('',(1.15996323728161,32.4,2.8));
#8579=CARTESIAN_POINT('Origin',(1.5,32.,2.8));
#8580=CARTESIAN_POINT('',(1.15996323728161,32.4,6.5));
#8581=CARTESIAN_POINT('',(1.15996323728161,32.4,2.8));
#8582=CARTESIAN_POINT('Origin',(1.5,32.,6.5));
#8583=CARTESIAN_POINT('Origin',(0.,31.6,4.6));
#8584=CARTESIAN_POINT('',(2.2,31.6,2.8));
#8585=CARTESIAN_POINT('',(0.,31.6,2.8));
#8586=CARTESIAN_POINT('',(2.2,31.6,6.5));
#8587=CARTESIAN_POINT('',(2.2,31.6,2.7));
#8588=CARTESIAN_POINT('',(2.2,31.6,6.5));
#8589=CARTESIAN_POINT('Origin',(0.,31.6,4.6));
#8590=CARTESIAN_POINT('',(-1.15996323728161,31.6,6.5));
#8591=CARTESIAN_POINT('',(2.2,31.6,6.5));
#8592=CARTESIAN_POINT('',(-1.15996323728161,31.6,2.8));
#8593=CARTESIAN_POINT('',(-1.15996323728161,31.6,2.8));
#8594=CARTESIAN_POINT('',(0.,31.6,2.8));
#8595=CARTESIAN_POINT('',(-0.505,31.6,4.5));
#8596=CARTESIAN_POINT('Origin',(0.,31.6,4.5));
#8597=CARTESIAN_POINT('Origin',(-2.2,31.6,6.5));
#8598=CARTESIAN_POINT('',(2.2,32.4,6.5));
#8599=CARTESIAN_POINT('',(2.2,31.6,6.5));
#8600=CARTESIAN_POINT('',(2.2,32.4,6.5));
#8601=CARTESIAN_POINT('Origin',(-2.2,31.6,6.5));
#8602=CARTESIAN_POINT('',(-1.15996323728161,32.4,6.5));
#8603=CARTESIAN_POINT('',(2.2,32.4,6.5));
#8604=CARTESIAN_POINT('Origin',(-1.5,32.,6.5));
#8605=CARTESIAN_POINT('Origin',(0.,32.4,4.6));
#8606=CARTESIAN_POINT('',(2.2,32.4,2.8));
#8607=CARTESIAN_POINT('',(2.2,32.4,2.7));
#8608=CARTESIAN_POINT('',(0.,32.4,2.8));
#8609=CARTESIAN_POINT('Origin',(0.,32.4,4.6));
#8610=CARTESIAN_POINT('',(-1.15996323728161,32.4,2.8));
#8611=CARTESIAN_POINT('',(0.,32.4,2.8));
#8612=CARTESIAN_POINT('',(-1.15996323728161,32.4,2.8));
#8613=CARTESIAN_POINT('',(-0.505,32.4,4.5));
#8614=CARTESIAN_POINT('Origin',(0.,32.4,4.5));
#8615=CARTESIAN_POINT('Origin',(1.5,32.,1.9));
#8616=CARTESIAN_POINT('',(1.225,32.,2.));
#8617=CARTESIAN_POINT('Origin',(1.5,32.,2.));
#8618=CARTESIAN_POINT('',(1.225,32.,2.8));
#8619=CARTESIAN_POINT('',(1.225,32.,1.9));
#8620=CARTESIAN_POINT('Origin',(1.5,32.,2.8));
#8621=CARTESIAN_POINT('Origin',(-1.5,32.,2.8));
#8622=CARTESIAN_POINT('',(-1.84003676271839,32.4,6.5));
#8623=CARTESIAN_POINT('',(-1.84003676271839,32.4,2.8));
#8624=CARTESIAN_POINT('',(-1.84003676271839,32.4,2.8));
#8625=CARTESIAN_POINT('',(-1.84003676271839,31.6,6.5));
#8626=CARTESIAN_POINT('Origin',(-1.5,32.,6.5));
#8627=CARTESIAN_POINT('',(-1.84003676271839,31.6,2.8));
#8628=CARTESIAN_POINT('',(-1.84003676271839,31.6,2.8));
#8629=CARTESIAN_POINT('Origin',(-1.5,32.,2.8));
#8630=CARTESIAN_POINT('Origin',(-1.5,32.,2.8));
#8631=CARTESIAN_POINT('Origin',(-1.5,32.,2.8));
#8632=CARTESIAN_POINT('Origin',(0.,32.4,4.6));
#8633=CARTESIAN_POINT('',(-2.2,32.4,2.8));
#8634=CARTESIAN_POINT('',(0.,32.4,2.8));
#8635=CARTESIAN_POINT('',(-2.2,32.4,6.5));
#8636=CARTESIAN_POINT('',(-2.2,32.4,6.5));
#8637=CARTESIAN_POINT('',(2.2,32.4,6.5));
#8638=CARTESIAN_POINT('Origin',(-2.2,31.6,6.5));
#8639=CARTESIAN_POINT('',(-2.2,31.6,6.5));
#8640=CARTESIAN_POINT('',(-2.2,31.6,6.5));
#8641=CARTESIAN_POINT('',(2.2,31.6,6.5));
#8642=CARTESIAN_POINT('Origin',(0.,31.6,4.6));
#8643=CARTESIAN_POINT('',(-2.2,31.6,2.8));
#8644=CARTESIAN_POINT('',(-2.2,31.6,6.5));
#8645=CARTESIAN_POINT('',(0.,31.6,2.8));
#8646=CARTESIAN_POINT('Origin',(-1.5,32.,1.9));
#8647=CARTESIAN_POINT('',(-1.775,32.,2.));
#8648=CARTESIAN_POINT('Origin',(-1.5,32.,2.));
#8649=CARTESIAN_POINT('',(-1.775,32.,2.8));
#8650=CARTESIAN_POINT('',(-1.775,32.,1.9));
#8651=CARTESIAN_POINT('Origin',(-1.5,32.,2.8));
#8652=CARTESIAN_POINT('Origin',(0.,31.5,4.5));
#8653=CARTESIAN_POINT('',(-0.505,31.5,4.5));
#8654=CARTESIAN_POINT('Origin',(2.2,31.6,6.5));
#8655=CARTESIAN_POINT('',(2.2,31.8,2.8));
#8656=CARTESIAN_POINT('Origin',(-2.2,31.6,2.7));
#8657=CARTESIAN_POINT('',(-2.2,31.8,2.8));
#8658=CARTESIAN_POINT('Origin',(3.,33.2,2.));
#8659=CARTESIAN_POINT('',(3.,33.2,2.));
#8660=CARTESIAN_POINT('',(-3.,33.2,2.));
#8661=CARTESIAN_POINT('',(3.,33.2,2.));
#8662=CARTESIAN_POINT('',(-3.,33.2,2.8));
#8663=CARTESIAN_POINT('',(-3.,33.2,2.));
#8664=CARTESIAN_POINT('',(3.,33.2,2.8));
#8665=CARTESIAN_POINT('',(3.,33.2,2.8));
#8666=CARTESIAN_POINT('',(3.,33.2,2.));
#8667=CARTESIAN_POINT('Origin',(3.,30.8,2.));
#8668=CARTESIAN_POINT('',(3.,30.8,2.));
#8669=CARTESIAN_POINT('',(3.,30.8,2.));
#8670=CARTESIAN_POINT('',(3.,30.8,2.8));
#8671=CARTESIAN_POINT('',(3.,30.8,2.8));
#8672=CARTESIAN_POINT('',(3.,30.8,2.));
#8673=CARTESIAN_POINT('Origin',(-3.,30.8,2.));
#8674=CARTESIAN_POINT('',(-3.,30.8,2.));
#8675=CARTESIAN_POINT('',(-3.,30.8,2.));
#8676=CARTESIAN_POINT('',(-3.,30.8,2.8));
#8677=CARTESIAN_POINT('',(-3.,30.8,2.8));
#8678=CARTESIAN_POINT('',(-3.,30.8,2.));
#8679=CARTESIAN_POINT('Origin',(-3.,33.2,2.));
#8680=CARTESIAN_POINT('',(-3.,33.2,2.));
#8681=CARTESIAN_POINT('',(-3.,33.2,2.8));
#8682=CARTESIAN_POINT('Origin',(0.,32.,2.8));
#8683=CARTESIAN_POINT('Origin',(0.,32.,2.));
#9578=UNCERTAINTY_MEASURE_WITH_UNIT(LENGTH_MEASURE(0.001),#9623,
'DISTANCE_ACCURACY_VALUE',
'Maximum model space distance between geometric entities at asserted c
onnectivities');
#9592=UNCERTAINTY_MEASURE_WITH_UNIT(LENGTH_MEASURE(0.001),#9623,
'DISTANCE_ACCURACY_VALUE',
'Maximum model space distance between geometric entities at asserted c
onnectivities');
#9608=(
GEOMETRIC_REPRESENTATION_CONTEXT(3)
GLOBAL_UNCERTAINTY_ASSIGNED_CONTEXT((#9578))
GLOBAL_UNIT_ASSIGNED_CONTEXT((#9623,#9625,#9626))
REPRESENTATION_CONTEXT('','3D')
);
#9622=(
GEOMETRIC_REPRESENTATION_CONTEXT(3)
GLOBAL_UNCERTAINTY_ASSIGNED_CONTEXT((#9592))
GLOBAL_UNIT_ASSIGNED_CONTEXT((#9623,#9625,#9626))
REPRESENTATION_CONTEXT('','3D')
);
#9623=(
LENGTH_UNIT()
NAMED_UNIT(*)
SI_UNIT(.CENTI.,.METRE.)
);
#9625=(
NAMED_UNIT(*)
PLANE_ANGLE_UNIT()
SI_UNIT($,.RADIAN.)
);
#9626=(
NAMED_UNIT(*)
SI_UNIT($,.STERADIAN.)
SOLID_ANGLE_UNIT()
);
#9642=SHAPE_DEFINITION_REPRESENTATION(#9676,#9759);
#9676=PRODUCT_DEFINITION_SHAPE('',$,#9789);
#9759=SHAPE_REPRESENTATION('',(#5757),#9608);
#9773=PRODUCT_DEFINITION_CONTEXT('part definition',#9862,'design');
#9789=PRODUCT_DEFINITION('Sliding axle block (1)',
'Sliding axle block (1)',#9818,#9773);
#9818=PRODUCT_DEFINITION_FORMATION('',$,#9879);
#9862=APPLICATION_CONTEXT(
'Core Data for Automotive Mechanical Design Process');
#9863=PRODUCT_CONTEXT('part definition',#9862,'mechanical');
#9879=PRODUCT('Sliding axle block (1)','Sliding axle block (1)',
'Sliding axle block (1)',(#9863));
#9956=COLOUR_RGB('Grey',0.48,0.52,0.57);
#9957=FILL_AREA_STYLE_COLOUR('',#9956);
#9958=FILL_AREA_STYLE('',(#9957));
#9959=SURFACE_STYLE_FILL_AREA(#9958);
#9960=SURFACE_SIDE_STYLE('',(#9959));
#9961=SURFACE_STYLE_USAGE(.BOTH.,#9960);
#9962=PRESENTATION_STYLE_ASSIGNMENT((#9961));
ENDSEC;
END-ISO-10303-21;
